ISO-10303-21;
HEADER;
FILE_DESCRIPTION (('STEP AP203'),
    '1' );
FILE_NAME ('bench vise6-.step',
    '2026-10-07T23:37:23',
    ( '' ),
    ( '' ),
    'SwSTEP 2.0',
    'SolidWorks 2024',
    '' );
FILE_SCHEMA (( 'AUTOMOTIVE_DESIGN' ));
ENDSEC;

DATA;
#2=DIRECTION ( 'NONE',  ( 1.000000000000000000, 0.000000000000000000, 0.000000000000000000 ) ) ;
#363=FACE_OUTER_BOUND ( 'NONE', #4172, .T. ) ;
#405=DIRECTION ( 'NONE',  ( 1.000000000000000000, 0.000000000000000000, -0.000000000000000000 ) ) ;
#493=ADVANCED_FACE ( 'NONE', ( #3931 ), #2144, .T. ) ;
#586=VERTEX_POINT ( 'NONE', #4805 ) ;
#720=( GEOMETRIC_REPRESENTATION_CONTEXT ( 3 ) GLOBAL_UNCERTAINTY_ASSIGNED_CONTEXT ( ( #5951 ) ) GLOBAL_UNIT_ASSIGNED_CONTEXT ( ( #5359, #4836, #7454 ) ) REPRESENTATION_CONTEXT ( 'NONE', 'WORKASPACE' ) );
#794=DIRECTION ( 'NONE',  ( 0.000000000000000000, 0.000000000000000000, 1.000000000000000000 ) ) ;
#1027=CARTESIAN_POINT ( 'NONE',  ( 2.537499998660271761, 3.550000000000001155, -0.3883559095726498156 ) ) ;
#1030=PRODUCT_DEFINITION ( 'UNKNOWN', '', #2798, #3569 ) ;
#1078=DIRECTION ( 'NONE',  ( 1.000000000000000000, 0.000000000000000000, 0.000000000000000000 ) ) ;
#1137=ADVANCED_FACE ( 'NONE', ( #363 ), #5351, .T. ) ;
#1147=CARTESIAN_POINT ( 'NONE',  ( 2.537499998660271761, 3.550000000000001155, -0.3883559095726498156 ) ) ;
#1227=CIRCLE ( 'NONE', #4488, 0.1875000000000006661 ) ;
#1432=PRODUCT ( 'bench vise6-', 'bench vise6-', '', ( #4190 ) ) ;
#1539=DIRECTION ( 'NONE',  ( 0.000000000000000000, 0.000000000000000000, 1.000000000000000000 ) ) ;
#1825=ORIENTED_EDGE ( 'NONE', *, *, #2675, .T. ) ;
#1992=CARTESIAN_POINT ( 'NONE',  ( 2.724999998660272205, 3.550000000000001155, -1.169467086614173645 ) ) ;
#2084=EDGE_CURVE ( 'NONE', #586, #5647, #5715, .T. ) ;
#2144=CYLINDRICAL_SURFACE ( 'NONE', #2566, 0.1875000000000006661 ) ;
#2187=ADVANCED_FACE ( 'N', ( #6754 ), #3640, .T. ) ;
#2273=AXIS2_PLACEMENT_3D ( 'NONE', #7794, #1539, #1078 ) ;
#2312=LINE ( 'NONE', #6002, #5928 ) ;
#2343=LENGTH_MEASURE_WITH_UNIT ( LENGTH_MEASURE( 0.02539999999999999897 ), #2951 );
#2458=DIRECTION ( 'NONE',  ( -1.000000000000000000, 0.000000000000000000, -0.000000000000000000 ) ) ;
#2564=DIMENSIONAL_EXPONENTS ( 1.000000000000000000, 0.000000000000000000, 0.000000000000000000, 0.000000000000000000, 0.000000000000000000, 0.000000000000000000, 0.000000000000000000 ) ;
#2566=AXIS2_PLACEMENT_3D ( 'NONE', #7796, #6412, #5755 ) ;
#2637=ORIENTED_EDGE ( 'NONE', *, *, #4052, .T. ) ;
#2674=CARTESIAN_POINT ( 'NONE',  ( 2.349999998660270872, 3.550000000000001155, -0.3883559095726498156 ) ) ;
#2675=EDGE_CURVE ( 'NONE', #2861, #586, #7083, .T. ) ;
#2724=EDGE_CURVE ( 'NONE', #5647, #586, #7162, .T. ) ;
#2772=VERTEX_POINT ( 'NONE', #7523 ) ;
#2798=PRODUCT_DEFINITION_FORMATION_WITH_SPECIFIED_SOURCE ( 'ANY', '', #1432, .NOT_KNOWN. ) ;
#2861=VERTEX_POINT ( 'NONE', #1992 ) ;
#2926=APPLICATION_CONTEXT ( 'configuration controlled 3d designs of mechanical parts and assemblies' ) ;
#2951=( LENGTH_UNIT ( ) NAMED_UNIT ( * ) SI_UNIT ( $, .METRE. ) );
#2977=CARTESIAN_POINT ( 'NONE',  ( 2.537499998660271761, 3.362500000000000711, -1.169467086614173645 ) ) ;
#3150=CARTESIAN_POINT ( 'NONE',  ( 2.537499998660271761, 3.550000000000001155, -1.169467086614173645 ) ) ;
#3292=DIRECTION ( 'NONE',  ( 1.000000000000000000, 0.000000000000000000, 0.000000000000000000 ) ) ;
#3337=FACE_OUTER_BOUND ( 'NONE', #7325, .T. ) ;
#3399=ORIENTED_EDGE ( 'NONE', *, *, #7579, .T. ) ;
#3430=ORIENTED_EDGE ( 'NONE', *, *, #2084, .F. ) ;
#3510=EDGE_LOOP ( 'NONE', ( #7556, #3399, #1825, #7048 ) ) ;
#3569=DESIGN_CONTEXT ( 'detailed design', #2926, 'design' ) ;
#3640=PLANE ( 'NONE',  #6373 ) ;
#3649=DIRECTION ( 'NONE',  ( -0.000000000000000000, -0.000000000000000000, -1.000000000000000000 ) ) ;
#3669=SHAPE_DEFINITION_REPRESENTATION ( #7354, #5548 ) ;
#3722=DIRECTION ( 'NONE',  ( 1.000000000000000000, 0.000000000000000000, 0.000000000000000000 ) ) ;
#3736=CARTESIAN_POINT ( 'NONE',  ( 0.000000000000000000, 0.000000000000000000, 0.000000000000000000 ) ) ;
#3832=CIRCLE ( 'NONE', #2273, 0.1875000000000006661 ) ;
#3931=FACE_OUTER_BOUND ( 'NONE', #3510, .T. ) ;
#4052=EDGE_CURVE ( 'NONE', #2861, #2772, #3832, .T. ) ;
#4172=EDGE_LOOP ( 'NONE', ( #3430, #4475 ) ) ;
#4190=MECHANICAL_CONTEXT ( 'NONE', #4821, 'mechanical' ) ;
#4255=SHAPE_REPRESENTATION_RELATIONSHIP ( 'NONE' , 'NONE' ,  #5548, #6817 ) ;
#4361=DIRECTION ( 'NONE',  ( 0.000000000000000000, 0.000000000000000000, -1.000000000000000000 ) ) ;
#4365=ORIENTED_EDGE ( 'NONE', *, *, #2675, .F. ) ;
#4404=VECTOR ( 'NONE', #5183, 39.37007874015748143 ) ;
#4468=MANIFOLD_SOLID_BREP ( 'Imported1', #4774 ) ;
#4475=ORIENTED_EDGE ( 'NONE', *, *, #2724, .F. ) ;
#4488=AXIS2_PLACEMENT_3D ( 'NONE', #3150, #5641, #3722 ) ;
#4719=CYLINDRICAL_SURFACE ( 'NONE', #5655, 0.1875000000000006661 ) ;
#4774=CLOSED_SHELL ( 'NONE', ( #7230, #493, #1137, #2187 ) ) ;
#4805=CARTESIAN_POINT ( 'NONE',  ( 2.724999998660272205, 3.550000000000001155, -0.3883559095726498156 ) ) ;
#4821=APPLICATION_CONTEXT ( 'configuration controlled 3d designs of mechanical parts and assemblies' ) ;
#4836=( NAMED_UNIT ( * ) PLANE_ANGLE_UNIT ( ) SI_UNIT ( $, .RADIAN. ) );
#5051=ORIENTED_EDGE ( 'NONE', *, *, #7579, .F. ) ;
#5058=AXIS2_PLACEMENT_3D ( 'NONE', #1027, #6020, #405 ) ;
#5183=DIRECTION ( 'NONE',  ( 0.000000000000000000, 0.000000000000000000, 1.000000000000000000 ) ) ;
#5344=CARTESIAN_POINT ( 'NONE',  ( 2.537499998660271761, 3.550000000000001155, -0.3883559095726498156 ) ) ;
#5351=PLANE ( 'NONE',  #5058 ) ;
#5359=( CONVERSION_BASED_UNIT ( 'INCH', #2343 ) LENGTH_UNIT ( ) NAMED_UNIT ( #2564 ) );
#5548=SHAPE_REPRESENTATION ( 'bench vise6-', ( #7272 ), #720 ) ;
#5560=DIRECTION ( 'NONE',  ( 1.000000000000000000, 0.000000000000000000, 0.000000000000000000 ) ) ;
#5618=DIRECTION ( 'NONE',  ( 1.000000000000000000, 0.000000000000000000, 0.000000000000000000 ) ) ;
#5641=DIRECTION ( 'NONE',  ( 0.000000000000000000, 0.000000000000000000, 1.000000000000000000 ) ) ;
#5647=VERTEX_POINT ( 'NONE', #2674 ) ;
#5655=AXIS2_PLACEMENT_3D ( 'NONE', #7237, #794, #3292 ) ;
#5715=CIRCLE ( 'NONE', #6523, 0.1875000000000006661 ) ;
#5755=DIRECTION ( 'NONE',  ( 1.000000000000000000, 0.000000000000000000, 0.000000000000000000 ) ) ;
#5928=VECTOR ( 'NONE', #7371, 39.37007874015748143 ) ;
#5951=UNCERTAINTY_MEASURE_WITH_UNIT (LENGTH_MEASURE( 1.000000000000000082E-05 ), #5359, 'distance_accuracy_value', 'NONE');
#6002=CARTESIAN_POINT ( 'NONE',  ( 2.349999998660270872, 3.550000000000001155, -1.169467086614173645 ) ) ;
#6020=DIRECTION ( 'NONE',  ( 0.000000000000000000, 0.000000000000000000, 1.000000000000000000 ) ) ;
#6237=DIRECTION ( 'NONE',  ( 0.000000000000000000, 0.000000000000000000, 1.000000000000000000 ) ) ;
#6373=AXIS2_PLACEMENT_3D ( 'NONE', #2977, #4361, #2458 ) ;
#6412=DIRECTION ( 'NONE',  ( 0.000000000000000000, 0.000000000000000000, 1.000000000000000000 ) ) ;
#6523=AXIS2_PLACEMENT_3D ( 'NONE', #5344, #7901, #2 ) ;
#6590=EDGE_LOOP ( 'NONE', ( #7198, #5051 ) ) ;
#6754=FACE_OUTER_BOUND ( 'NONE', #6590, .T. ) ;
#6817=ADVANCED_BREP_SHAPE_REPRESENTATION ( '', ( #4468, #7272 ), #720 ) ;
#7035=AXIS2_PLACEMENT_3D ( 'NONE', #1147, #3649, #5560 ) ;
#7048=ORIENTED_EDGE ( 'NONE', *, *, #2084, .T. ) ;
#7052=ORIENTED_EDGE ( 'NONE', *, *, #7317, .T. ) ;
#7083=LINE ( 'NONE', #7766, #4404 ) ;
#7162=CIRCLE ( 'NONE', #7035, 0.1875000000000006661 ) ;
#7198=ORIENTED_EDGE ( 'NONE', *, *, #4052, .F. ) ;
#7230=ADVANCED_FACE ( 'NONE', ( #3337 ), #4719, .T. ) ;
#7237=CARTESIAN_POINT ( 'NONE',  ( 2.537499998660271761, 3.550000000000001155, -1.169467086614173645 ) ) ;
#7272=AXIS2_PLACEMENT_3D ( 'NONE', #3736, #6237, #5618 ) ;
#7317=EDGE_CURVE ( 'NONE', #2772, #5647, #2312, .T. ) ;
#7325=EDGE_LOOP ( 'NONE', ( #2637, #7052, #7458, #4365 ) ) ;
#7354=PRODUCT_DEFINITION_SHAPE ( 'NONE', 'NONE',  #1030 ) ;
#7371=DIRECTION ( 'NONE',  ( 0.000000000000000000, 0.000000000000000000, 1.000000000000000000 ) ) ;
#7454=( NAMED_UNIT ( * ) SI_UNIT ( $, .STERADIAN. ) SOLID_ANGLE_UNIT ( ) );
#7458=ORIENTED_EDGE ( 'NONE', *, *, #2724, .T. ) ;
#7523=CARTESIAN_POINT ( 'NONE',  ( 2.349999998660270872, 3.550000000000001155, -1.169467086614173645 ) ) ;
#7556=ORIENTED_EDGE ( 'NONE', *, *, #7317, .F. ) ;
#7579=EDGE_CURVE ( 'NONE', #2772, #2861, #1227, .T. ) ;
#7766=CARTESIAN_POINT ( 'NONE',  ( 2.724999998660272205, 3.550000000000001155, -1.169467086614173645 ) ) ;
#7794=CARTESIAN_POINT ( 'NONE',  ( 2.537499998660271761, 3.550000000000001155, -1.169467086614173645 ) ) ;
#7796=CARTESIAN_POINT ( 'NONE',  ( 2.537499998660271761, 3.550000000000001155, -1.169467086614173645 ) ) ;
#7901=DIRECTION ( 'NONE',  ( -0.000000000000000000, -0.000000000000000000, -1.000000000000000000 ) ) ;
#8220=COLOUR_RGB('Slate Gray', 0.72549020, 0.75294118, 0.79215686);
#8221=FILL_AREA_STYLE_COLOUR('',#8220);
#8222=FILL_AREA_STYLE('',(#8221));
#8223=SURFACE_STYLE_FILL_AREA(#8222);
#8224=SURFACE_SIDE_STYLE('',(#8223));
#8225=SURFACE_STYLE_USAGE(.BOTH.,#8224);
#8226=PRESENTATION_STYLE_ASSIGNMENT((#8225));
#8257=STYLED_ITEM('',(#8226),#4468);
#8258=MECHANICAL_DESIGN_GEOMETRIC_PRESENTATION_REPRESENTATION('',(#8257),#720);
ENDSEC;
END-ISO-10303-21;
